ISO-10303-21;
HEADER;
/* Generated by software containing ST-Developer
 * from STEP Tools, Inc. (www.steptools.com) 
 */

FILE_DESCRIPTION(
/* description */ ('Ratchet and pawl hand winch drum'),
/* implementation_level */ '2;1');

FILE_NAME(
/* name */ 'M8x25 Bolt.step',
/* time_stamp */ '2026-10-27T12:42:58-07:00',
/* author */ (''),
/* organization */ (''),
/* preprocessor_version */ 'ST-DEVELOPER v20.2',
/* originating_system */ 'Autodesk Translation Framework v15.17.0.0',
/* authorisation */ '');

FILE_SCHEMA (('AUTOMOTIVE_DESIGN { 1 0 10303 214 3 1 1 }'));
ENDSEC;

DATA;
#10=MECHANICAL_DESIGN_GEOMETRIC_PRESENTATION_REPRESENTATION('',(#408),#11801);
#11=CONICAL_SURFACE('',#7014,0.625,0.785398163397448);
#12=CONICAL_SURFACE('',#7018,0.635,0.785398163397449);
#13=CONICAL_SURFACE('',#7022,0.41,0.463647609000806);
#23=ORIENTED_CLOSED_SHELL('',*,#6285,.F.);
#26=BREP_WITH_VOIDS('Body1',#6286,(#23));
#339=SHAPE_REPRESENTATION_RELATIONSHIP('SRR','None',#11966,#373);
#373=ADVANCED_BREP_SHAPE_REPRESENTATION('',(#26),#11783);
#408=STYLED_ITEM('',(#12220),#26);
#562=FACE_BOUND('',#1487,.T.);
#704=PLANE('',#7002);
#705=PLANE('',#7003);
#706=PLANE('',#7004);
#707=PLANE('',#7005);
#708=PLANE('',#7006);
#709=PLANE('',#7007);
#710=PLANE('',#7008);
#711=PLANE('',#7009);
#712=PLANE('',#7010);
#713=PLANE('',#7012);
#714=PLANE('',#7020);
#1011=FACE_OUTER_BOUND('',#1473,.T.);
#1012=FACE_OUTER_BOUND('',#1474,.T.);
#1013=FACE_OUTER_BOUND('',#1475,.T.);
#1014=FACE_OUTER_BOUND('',#1476,.T.);
#1015=FACE_OUTER_BOUND('',#1477,.T.);
#1016=FACE_OUTER_BOUND('',#1478,.T.);
#1017=FACE_OUTER_BOUND('',#1479,.T.);
#1018=FACE_OUTER_BOUND('',#1480,.T.);
#1019=FACE_OUTER_BOUND('',#1481,.T.);
#1020=FACE_OUTER_BOUND('',#1482,.T.);
#1021=FACE_OUTER_BOUND('',#1483,.T.);
#1022=FACE_OUTER_BOUND('',#1484,.T.);
#1023=FACE_OUTER_BOUND('',#1485,.T.);
#1024=FACE_OUTER_BOUND('',#1486,.T.);
#1025=FACE_OUTER_BOUND('',#1488,.T.);
#1026=FACE_OUTER_BOUND('',#1489,.T.);
#1473=EDGE_LOOP('',(#4981,#4982,#4983,#4984));
#1474=EDGE_LOOP('',(#4985,#4986,#4987,#4988));
#1475=EDGE_LOOP('',(#4989,#4990,#4991,#4992));
#1476=EDGE_LOOP('',(#4993,#4994,#4995,#4996));
#1477=EDGE_LOOP('',(#4997,#4998,#4999,#5000));
#1478=EDGE_LOOP('',(#5001,#5002,#5003,#5004));
#1479=EDGE_LOOP('',(#5005,#5006,#5007,#5008,#5009,#5010));
#1480=EDGE_LOOP('',(#5011,#5012,#5013,#5014,#5015,#5016));
#1481=EDGE_LOOP('',(#5017));
#1482=EDGE_LOOP('',(#5018));
#1483=EDGE_LOOP('',(#5019,#5020,#5021,#5022));
#1484=EDGE_LOOP('',(#5023,#5024,#5025,#5026));
#1485=EDGE_LOOP('',(#5027,#5028,#5029,#5030));
#1486=EDGE_LOOP('',(#5031));
#1487=EDGE_LOOP('',(#5032));
#1488=EDGE_LOOP('',(#5033,#5034,#5035,#5036));
#1489=EDGE_LOOP('',(#5037,#5038,#5039,#5040));
#1912=LINE('',#10452,#2423);
#1913=LINE('',#10454,#2424);
#1914=LINE('',#10456,#2425);
#1915=LINE('',#10457,#2426);
#1916=LINE('',#10460,#2427);
#1917=LINE('',#10462,#2428);
#1918=LINE('',#10463,#2429);
#1919=LINE('',#10466,#2430);
#1920=LINE('',#10468,#2431);
#1921=LINE('',#10469,#2432);
#1922=LINE('',#10472,#2433);
#1923=LINE('',#10474,#2434);
#1924=LINE('',#10475,#2435);
#1925=LINE('',#10478,#2436);
#1926=LINE('',#10480,#2437);
#1927=LINE('',#10481,#2438);
#1928=LINE('',#10483,#2439);
#1929=LINE('',#10484,#2440);
#1930=LINE('',#10496,#2441);
#1931=LINE('',#10500,#2442);
#1932=LINE('',#10504,#2443);
#1933=LINE('',#10511,#2444);
#1934=LINE('',#10513,#2445);
#2423=VECTOR('',#8221,1.);
#2424=VECTOR('',#8222,1.);
#2425=VECTOR('',#8223,1.);
#2426=VECTOR('',#8224,1.);
#2427=VECTOR('',#8227,1.);
#2428=VECTOR('',#8228,1.);
#2429=VECTOR('',#8229,1.);
#2430=VECTOR('',#8232,1.);
#2431=VECTOR('',#8233,1.);
#2432=VECTOR('',#8234,1.);
#2433=VECTOR('',#8237,1.);
#2434=VECTOR('',#8238,1.);
#2435=VECTOR('',#8239,1.);
#2436=VECTOR('',#8242,1.);
#2437=VECTOR('',#8243,1.);
#2438=VECTOR('',#8244,1.);
#2439=VECTOR('',#8247,1.);
#2440=VECTOR('',#8248,1.);
#2441=VECTOR('',#8265,0.625);
#2442=VECTOR('',#8270,0.65);
#2443=VECTOR('',#8275,0.635);
#2444=VECTOR('',#8284,0.41);
#2445=VECTOR('',#8287,0.4);
#2847=CIRCLE('',#7011,0.3933);
#2848=CIRCLE('',#7013,0.6);
#2849=CIRCLE('',#7015,0.65);
#2850=CIRCLE('',#7017,0.65);
#2851=CIRCLE('',#7019,0.62);
#2852=CIRCLE('',#7021,0.42);
#2853=CIRCLE('',#7023,0.3933);
#3194=VERTEX_POINT('',#10450);
#3195=VERTEX_POINT('',#10451);
#3196=VERTEX_POINT('',#10453);
#3197=VERTEX_POINT('',#10455);
#3198=VERTEX_POINT('',#10459);
#3199=VERTEX_POINT('',#10461);
#3200=VERTEX_POINT('',#10465);
#3201=VERTEX_POINT('',#10467);
#3202=VERTEX_POINT('',#10471);
#3203=VERTEX_POINT('',#10473);
#3204=VERTEX_POINT('',#10477);
#3205=VERTEX_POINT('',#10479);
#3206=VERTEX_POINT('',#10488);
#3207=VERTEX_POINT('',#10491);
#3208=VERTEX_POINT('',#10494);
#3209=VERTEX_POINT('',#10498);
#3210=VERTEX_POINT('',#10502);
#3211=VERTEX_POINT('',#10506);
#3212=VERTEX_POINT('',#10509);
#3834=EDGE_CURVE('',#3194,#3195,#1912,.T.);
#3835=EDGE_CURVE('',#3195,#3196,#1913,.T.);
#3836=EDGE_CURVE('',#3196,#3197,#1914,.T.);
#3837=EDGE_CURVE('',#3194,#3197,#1915,.T.);
#3838=EDGE_CURVE('',#3195,#3198,#1916,.T.);
#3839=EDGE_CURVE('',#3198,#3199,#1917,.T.);
#3840=EDGE_CURVE('',#3199,#3196,#1918,.T.);
#3841=EDGE_CURVE('',#3198,#3200,#1919,.T.);
#3842=EDGE_CURVE('',#3200,#3201,#1920,.T.);
#3843=EDGE_CURVE('',#3201,#3199,#1921,.T.);
#3844=EDGE_CURVE('',#3200,#3202,#1922,.T.);
#3845=EDGE_CURVE('',#3202,#3203,#1923,.T.);
#3846=EDGE_CURVE('',#3203,#3201,#1924,.T.);
#3847=EDGE_CURVE('',#3202,#3204,#1925,.T.);
#3848=EDGE_CURVE('',#3204,#3205,#1926,.T.);
#3849=EDGE_CURVE('',#3205,#3203,#1927,.T.);
#3850=EDGE_CURVE('',#3204,#3194,#1928,.T.);
#3851=EDGE_CURVE('',#3197,#3205,#1929,.T.);
#3852=EDGE_CURVE('',#3206,#3206,#2847,.T.);
#3853=EDGE_CURVE('',#3207,#3207,#2848,.T.);
#3854=EDGE_CURVE('',#3208,#3208,#2849,.T.);
#3855=EDGE_CURVE('',#3208,#3207,#1930,.T.);
#3856=EDGE_CURVE('',#3209,#3209,#2850,.T.);
#3857=EDGE_CURVE('',#3209,#3208,#1931,.T.);
#3858=EDGE_CURVE('',#3210,#3210,#2851,.T.);
#3859=EDGE_CURVE('',#3210,#3209,#1932,.T.);
#3860=EDGE_CURVE('',#3211,#3211,#2852,.T.);
#3861=EDGE_CURVE('',#3212,#3212,#2853,.F.);
#3862=EDGE_CURVE('',#3212,#3211,#1933,.T.);
#3863=EDGE_CURVE('',#3206,#3212,#1934,.T.);
#4981=ORIENTED_EDGE('',*,*,#3834,.T.);
#4982=ORIENTED_EDGE('',*,*,#3835,.T.);
#4983=ORIENTED_EDGE('',*,*,#3836,.T.);
#4984=ORIENTED_EDGE('',*,*,#3837,.F.);
#4985=ORIENTED_EDGE('',*,*,#3838,.T.);
#4986=ORIENTED_EDGE('',*,*,#3839,.T.);
#4987=ORIENTED_EDGE('',*,*,#3840,.T.);
#4988=ORIENTED_EDGE('',*,*,#3835,.F.);
#4989=ORIENTED_EDGE('',*,*,#3841,.T.);
#4990=ORIENTED_EDGE('',*,*,#3842,.T.);
#4991=ORIENTED_EDGE('',*,*,#3843,.T.);
#4992=ORIENTED_EDGE('',*,*,#3839,.F.);
#4993=ORIENTED_EDGE('',*,*,#3844,.T.);
#4994=ORIENTED_EDGE('',*,*,#3845,.T.);
#4995=ORIENTED_EDGE('',*,*,#3846,.T.);
#4996=ORIENTED_EDGE('',*,*,#3842,.F.);
#4997=ORIENTED_EDGE('',*,*,#3847,.T.);
#4998=ORIENTED_EDGE('',*,*,#3848,.T.);
#4999=ORIENTED_EDGE('',*,*,#3849,.T.);
#5000=ORIENTED_EDGE('',*,*,#3845,.F.);
#5001=ORIENTED_EDGE('',*,*,#3850,.T.);
#5002=ORIENTED_EDGE('',*,*,#3837,.T.);
#5003=ORIENTED_EDGE('',*,*,#3851,.T.);
#5004=ORIENTED_EDGE('',*,*,#3848,.F.);
#5005=ORIENTED_EDGE('',*,*,#3850,.F.);
#5006=ORIENTED_EDGE('',*,*,#3847,.F.);
#5007=ORIENTED_EDGE('',*,*,#3844,.F.);
#5008=ORIENTED_EDGE('',*,*,#3841,.F.);
#5009=ORIENTED_EDGE('',*,*,#3838,.F.);
#5010=ORIENTED_EDGE('',*,*,#3834,.F.);
#5011=ORIENTED_EDGE('',*,*,#3851,.F.);
#5012=ORIENTED_EDGE('',*,*,#3836,.F.);
#5013=ORIENTED_EDGE('',*,*,#3840,.F.);
#5014=ORIENTED_EDGE('',*,*,#3843,.F.);
#5015=ORIENTED_EDGE('',*,*,#3846,.F.);
#5016=ORIENTED_EDGE('',*,*,#3849,.F.);
#5017=ORIENTED_EDGE('',*,*,#3852,.F.);
#5018=ORIENTED_EDGE('',*,*,#3853,.F.);
#5019=ORIENTED_EDGE('',*,*,#3854,.F.);
#5020=ORIENTED_EDGE('',*,*,#3855,.T.);
#5021=ORIENTED_EDGE('',*,*,#3853,.T.);
#5022=ORIENTED_EDGE('',*,*,#3855,.F.);
#5023=ORIENTED_EDGE('',*,*,#3856,.F.);
#5024=ORIENTED_EDGE('',*,*,#3857,.T.);
#5025=ORIENTED_EDGE('',*,*,#3854,.T.);
#5026=ORIENTED_EDGE('',*,*,#3857,.F.);
#5027=ORIENTED_EDGE('',*,*,#3858,.F.);
#5028=ORIENTED_EDGE('',*,*,#3859,.T.);
#5029=ORIENTED_EDGE('',*,*,#3856,.T.);
#5030=ORIENTED_EDGE('',*,*,#3859,.F.);
#5031=ORIENTED_EDGE('',*,*,#3858,.T.);
#5032=ORIENTED_EDGE('',*,*,#3860,.F.);
#5033=ORIENTED_EDGE('',*,*,#3861,.F.);
#5034=ORIENTED_EDGE('',*,*,#3862,.T.);
#5035=ORIENTED_EDGE('',*,*,#3860,.T.);
#5036=ORIENTED_EDGE('',*,*,#3862,.F.);
#5037=ORIENTED_EDGE('',*,*,#3852,.T.);
#5038=ORIENTED_EDGE('',*,*,#3863,.T.);
#5039=ORIENTED_EDGE('',*,*,#3861,.T.);
#5040=ORIENTED_EDGE('',*,*,#3863,.F.);
#5873=CYLINDRICAL_SURFACE('',#7016,0.65);
#5874=CYLINDRICAL_SURFACE('',#7024,0.3933);
#6081=ADVANCED_FACE('',(#1011),#704,.F.);
#6082=ADVANCED_FACE('',(#1012),#705,.F.);
#6083=ADVANCED_FACE('',(#1013),#706,.F.);
#6084=ADVANCED_FACE('',(#1014),#707,.F.);
#6085=ADVANCED_FACE('',(#1015),#708,.F.);
#6086=ADVANCED_FACE('',(#1016),#709,.F.);
#6087=ADVANCED_FACE('',(#1017),#710,.F.);
#6088=ADVANCED_FACE('',(#1018),#711,.F.);
#6089=ADVANCED_FACE('',(#1019),#712,.F.);
#6090=ADVANCED_FACE('',(#1020),#713,.T.);
#6091=ADVANCED_FACE('',(#1021),#11,.T.);
#6092=ADVANCED_FACE('',(#1022),#5873,.T.);
#6093=ADVANCED_FACE('',(#1023),#12,.T.);
#6094=ADVANCED_FACE('',(#1024,#562),#714,.T.);
#6095=ADVANCED_FACE('',(#1025),#13,.T.);
#6096=ADVANCED_FACE('',(#1026),#5874,.T.);
#6285=CLOSED_SHELL('',(#6081,#6082,#6083,#6084,#6085,#6086,#6087,#6088));
#6286=CLOSED_SHELL('',(#6089,#6090,#6091,#6092,#6093,#6094,#6095,#6096));
#7001=AXIS2_PLACEMENT_3D('',#10448,#8217,#8218);
#7002=AXIS2_PLACEMENT_3D('',#10449,#8219,#8220);
#7003=AXIS2_PLACEMENT_3D('',#10458,#8225,#8226);
#7004=AXIS2_PLACEMENT_3D('',#10464,#8230,#8231);
#7005=AXIS2_PLACEMENT_3D('',#10470,#8235,#8236);
#7006=AXIS2_PLACEMENT_3D('',#10476,#8240,#8241);
#7007=AXIS2_PLACEMENT_3D('',#10482,#8245,#8246);
#7008=AXIS2_PLACEMENT_3D('',#10485,#8249,#8250);
#7009=AXIS2_PLACEMENT_3D('',#10486,#8251,#8252);
#7010=AXIS2_PLACEMENT_3D('',#10487,#8253,#8254);
#7011=AXIS2_PLACEMENT_3D('',#10489,#8255,#8256);
#7012=AXIS2_PLACEMENT_3D('',#10490,#8257,#8258);
#7013=AXIS2_PLACEMENT_3D('',#10492,#8259,#8260);
#7014=AXIS2_PLACEMENT_3D('',#10493,#8261,#8262);
#7015=AXIS2_PLACEMENT_3D('',#10495,#8263,#8264);
#7016=AXIS2_PLACEMENT_3D('',#10497,#8266,#8267);
#7017=AXIS2_PLACEMENT_3D('',#10499,#8268,#8269);
#7018=AXIS2_PLACEMENT_3D('',#10501,#8271,#8272);
#7019=AXIS2_PLACEMENT_3D('',#10503,#8273,#8274);
#7020=AXIS2_PLACEMENT_3D('',#10505,#8276,#8277);
#7021=AXIS2_PLACEMENT_3D('',#10507,#8278,#8279);
#7022=AXIS2_PLACEMENT_3D('',#10508,#8280,#8281);
#7023=AXIS2_PLACEMENT_3D('',#10510,#8282,#8283);
#7024=AXIS2_PLACEMENT_3D('',#10512,#8285,#8286);
#8217=DIRECTION('axis',(0.,0.,1.));
#8218=DIRECTION('refdir',(1.,0.,0.));
#8219=DIRECTION('center_axis',(0.866025403784439,0.,-0.5));
#8220=DIRECTION('ref_axis',(0.5,0.,0.866025403784439));
#8221=DIRECTION('',(-0.5,0.,-0.866025403784439));
#8222=DIRECTION('',(0.,-1.,0.));
#8223=DIRECTION('',(0.5,0.,0.866025403784439));
#8224=DIRECTION('',(0.,-1.,0.));
#8225=DIRECTION('center_axis',(1.60246890531964E-16,0.,-1.));
#8226=DIRECTION('ref_axis',(1.,0.,1.60246890531964E-16));
#8227=DIRECTION('',(-1.,0.,-1.60246890531964E-16));
#8228=DIRECTION('',(0.,-1.,0.));
#8229=DIRECTION('',(1.,0.,1.60246890531964E-16));
#8230=DIRECTION('center_axis',(-0.866025403784439,0.,-0.5));
#8231=DIRECTION('ref_axis',(0.5,0.,-0.866025403784439));
#8232=DIRECTION('',(-0.5,0.,0.866025403784439));
#8233=DIRECTION('',(0.,-1.,0.));
#8234=DIRECTION('',(0.5,0.,-0.866025403784439));
#8235=DIRECTION('center_axis',(-0.866025403784439,0.,0.5));
#8236=DIRECTION('ref_axis',(-0.5,0.,-0.866025403784439));
#8237=DIRECTION('',(0.5,0.,0.866025403784439));
#8238=DIRECTION('',(0.,-1.,0.));
#8239=DIRECTION('',(-0.5,0.,-0.866025403784439));
#8240=DIRECTION('center_axis',(-1.60246890531964E-16,0.,1.));
#8241=DIRECTION('ref_axis',(-1.,0.,-1.60246890531964E-16));
#8242=DIRECTION('',(1.,0.,1.60246890531964E-16));
#8243=DIRECTION('',(0.,-1.,0.));
#8244=DIRECTION('',(-1.,0.,-1.60246890531964E-16));
#8245=DIRECTION('center_axis',(0.866025403784439,0.,0.5));
#8246=DIRECTION('ref_axis',(-0.5,0.,0.866025403784439));
#8247=DIRECTION('',(0.5,0.,-0.866025403784439));
#8248=DIRECTION('',(-0.5,0.,0.866025403784439));
#8249=DIRECTION('center_axis',(0.,1.,0.));
#8250=DIRECTION('ref_axis',(1.,0.,0.));
#8251=DIRECTION('center_axis',(0.,-1.,0.));
#8252=DIRECTION('ref_axis',(0.,0.,-1.));
#8253=DIRECTION('center_axis',(0.,1.,0.));
#8254=DIRECTION('ref_axis',(1.,0.,0.));
#8255=DIRECTION('center_axis',(0.,1.,0.));
#8256=DIRECTION('ref_axis',(1.,0.,0.));
#8257=DIRECTION('center_axis',(0.,1.,0.));
#8258=DIRECTION('ref_axis',(0.,0.,1.));
#8259=DIRECTION('center_axis',(0.,-1.,0.));
#8260=DIRECTION('ref_axis',(1.,0.,0.));
#8261=DIRECTION('center_axis',(0.,-1.,0.));
#8262=DIRECTION('ref_axis',(1.,0.,0.));
#8263=DIRECTION('center_axis',(0.,-1.,0.));
#8264=DIRECTION('ref_axis',(1.,0.,0.));
#8265=DIRECTION('',(0.707106781186548,0.707106781186547,8.65956056235493E-17));
#8266=DIRECTION('center_axis',(0.,-1.,0.));
#8267=DIRECTION('ref_axis',(1.,0.,0.));
#8268=DIRECTION('center_axis',(0.,-1.,0.));
#8269=DIRECTION('ref_axis',(1.,0.,0.));
#8270=DIRECTION('',(0.,1.,0.));
#8271=DIRECTION('center_axis',(0.,1.,0.));
#8272=DIRECTION('ref_axis',(1.,0.,0.));
#8273=DIRECTION('center_axis',(0.,-1.,0.));
#8274=DIRECTION('ref_axis',(1.,0.,0.));
#8275=DIRECTION('',(-0.707106781186548,0.707106781186547,-8.65956056235494E-17));
#8276=DIRECTION('center_axis',(0.,-1.,0.));
#8277=DIRECTION('ref_axis',(0.,0.,-1.));
#8278=DIRECTION('center_axis',(0.,-1.,0.));
#8279=DIRECTION('ref_axis',(1.,0.,0.));
#8280=DIRECTION('center_axis',(0.,1.,0.));
#8281=DIRECTION('ref_axis',(1.,0.,0.));
#8282=DIRECTION('center_axis',(0.,1.,0.));
#8283=DIRECTION('ref_axis',(1.,0.,0.));
#8284=DIRECTION('',(-0.447213595499958,0.894427190999916,-5.47678698264203E-17));
#8285=DIRECTION('center_axis',(0.,-1.,0.));
#8286=DIRECTION('ref_axis',(1.,0.,0.));
#8287=DIRECTION('',(0.,1.,0.));
#10448=CARTESIAN_POINT('',(0.,0.,0.));
#10449=CARTESIAN_POINT('Origin',(0.173205080756888,-0.8,-0.3));
#10450=CARTESIAN_POINT('',(0.346410161513775,-0.8,0.));
#10451=CARTESIAN_POINT('',(0.173205080756888,-0.8,-0.3));
#10452=CARTESIAN_POINT('',(0.346410161513775,-0.8,0.));
#10453=CARTESIAN_POINT('',(0.173205080756888,-1.28,-0.3));
#10454=CARTESIAN_POINT('',(0.173205080756888,-0.8,-0.3));
#10455=CARTESIAN_POINT('',(0.346410161513775,-1.28,0.));
#10456=CARTESIAN_POINT('',(0.346410161513775,-1.28,0.));
#10457=CARTESIAN_POINT('',(0.346410161513775,-0.8,0.));
#10458=CARTESIAN_POINT('Origin',(-0.173205080756888,-0.8,-0.3));
#10459=CARTESIAN_POINT('',(-0.173205080756888,-0.8,-0.3));
#10460=CARTESIAN_POINT('',(0.173205080756888,-0.8,-0.3));
#10461=CARTESIAN_POINT('',(-0.173205080756888,-1.28,-0.3));
#10462=CARTESIAN_POINT('',(-0.173205080756888,-0.8,-0.3));
#10463=CARTESIAN_POINT('',(0.173205080756888,-1.28,-0.3));
#10464=CARTESIAN_POINT('Origin',(-0.346410161513775,-0.8,-5.55111512312578E-17));
#10465=CARTESIAN_POINT('',(-0.346410161513775,-0.8,-4.24230095489963E-17));
#10466=CARTESIAN_POINT('',(-0.173205080756888,-0.8,-0.3));
#10467=CARTESIAN_POINT('',(-0.346410161513775,-1.28,-5.55111512312578E-17));
#10468=CARTESIAN_POINT('',(-0.346410161513775,-0.8,-4.24230095489963E-17));
#10469=CARTESIAN_POINT('',(-0.173205080756888,-1.28,-0.3));
#10470=CARTESIAN_POINT('Origin',(-0.173205080756888,-0.8,0.3));
#10471=CARTESIAN_POINT('',(-0.173205080756888,-0.8,0.3));
#10472=CARTESIAN_POINT('',(-0.346410161513775,-0.8,-4.24230095489963E-17));
#10473=CARTESIAN_POINT('',(-0.173205080756888,-1.28,0.3));
#10474=CARTESIAN_POINT('',(-0.173205080756888,-0.8,0.3));
#10475=CARTESIAN_POINT('',(-0.346410161513775,-1.28,-4.24230095489963E-17));
#10476=CARTESIAN_POINT('Origin',(0.173205080756888,-0.8,0.3));
#10477=CARTESIAN_POINT('',(0.173205080756888,-0.8,0.3));
#10478=CARTESIAN_POINT('',(-0.173205080756888,-0.8,0.3));
#10479=CARTESIAN_POINT('',(0.173205080756888,-1.28,0.3));
#10480=CARTESIAN_POINT('',(0.173205080756888,-0.8,0.3));
#10481=CARTESIAN_POINT('',(-0.173205080756888,-1.28,0.3));
#10482=CARTESIAN_POINT('Origin',(0.346410161513775,-0.8,0.));
#10483=CARTESIAN_POINT('',(0.173205080756888,-0.8,0.3));
#10484=CARTESIAN_POINT('',(0.173205080756888,-1.28,0.3));
#10485=CARTESIAN_POINT('Origin',(0.,-0.8,-5.55111512312578E-17));
#10486=CARTESIAN_POINT('Origin',(0.,-1.28,-5.55111512312578E-17));
#10487=CARTESIAN_POINT('Origin',(0.,-2.5,0.));
#10488=CARTESIAN_POINT('',(-0.3933,-2.5,4.81653586104654E-17));
#10489=CARTESIAN_POINT('Origin',(0.,-2.5,0.));
#10490=CARTESIAN_POINT('Origin',(0.6,0.8,0.));
#10491=CARTESIAN_POINT('',(-0.6,0.8,-7.34788079488412E-17));
#10492=CARTESIAN_POINT('Origin',(0.,0.8,0.));
#10493=CARTESIAN_POINT('Origin',(0.,0.775,0.));
#10494=CARTESIAN_POINT('',(-0.65,0.75,-7.9602041944578E-17));
#10495=CARTESIAN_POINT('Origin',(0.,0.75,0.));
#10496=CARTESIAN_POINT('',(-0.625,0.775,-7.65404249467096E-17));
#10497=CARTESIAN_POINT('Origin',(0.,0.39,0.));
#10498=CARTESIAN_POINT('',(-0.65,0.0299999999999998,-7.9602041944578E-17));
#10499=CARTESIAN_POINT('Origin',(0.,0.0299999999999998,0.));
#10500=CARTESIAN_POINT('',(-0.65,0.39,-7.9602041944578E-17));
#10501=CARTESIAN_POINT('Origin',(0.,0.0150000000000001,0.));
#10502=CARTESIAN_POINT('',(-0.62,5.89805981832114E-17,-7.59281015471359E-17));
#10503=CARTESIAN_POINT('Origin',(0.,0.,0.));
#10504=CARTESIAN_POINT('',(-0.635,0.0150000000000001,-7.77650717458569E-17));
#10505=CARTESIAN_POINT('Origin',(0.42,0.,0.));
#10506=CARTESIAN_POINT('',(-0.42,-3.46944695195361E-18,-5.14351655641888E-17));
#10507=CARTESIAN_POINT('Origin',(0.,0.,0.));
#10508=CARTESIAN_POINT('Origin',(0.,-0.02,0.));
#10509=CARTESIAN_POINT('',(-0.3933,-0.0534000000000001,4.81653586104654E-17));
#10510=CARTESIAN_POINT('Origin',(0.,-0.0534000000000001,0.));
#10511=CARTESIAN_POINT('',(-0.41,-0.02,-5.02105187650415E-17));
#10512=CARTESIAN_POINT('Origin',(0.,-1.48,0.));
#10513=CARTESIAN_POINT('',(-0.3933,-1.48,-4.81653586104654E-17));
#11743=UNCERTAINTY_MEASURE_WITH_UNIT(LENGTH_MEASURE(0.001),#11802,
'DISTANCE_ACCURACY_VALUE',
'Maximum model space distance between geometric entities at asserted c
onnectivities');
#11761=UNCERTAINTY_MEASURE_WITH_UNIT(LENGTH_MEASURE(0.001),#11802,
'DISTANCE_ACCURACY_VALUE',
'Maximum model space distance between geometric entities at asserted c
onnectivities');
#11783=(
GEOMETRIC_REPRESENTATION_CONTEXT(3)
GLOBAL_UNCERTAINTY_ASSIGNED_CONTEXT((#11743))
GLOBAL_UNIT_ASSIGNED_CONTEXT((#11802,#11804,#11805))
REPRESENTATION_CONTEXT('','3D')
);
#11801=(
GEOMETRIC_REPRESENTATION_CONTEXT(3)
GLOBAL_UNCERTAINTY_ASSIGNED_CONTEXT((#11761))
GLOBAL_UNIT_ASSIGNED_CONTEXT((#11802,#11804,#11805))
REPRESENTATION_CONTEXT('','3D')
);
#11802=(
LENGTH_UNIT()
NAMED_UNIT(*)
SI_UNIT(.CENTI.,.METRE.)
);
#11804=(
NAMED_UNIT(*)
PLANE_ANGLE_UNIT()
SI_UNIT($,.RADIAN.)
);
#11805=(
NAMED_UNIT(*)
SI_UNIT($,.STERADIAN.)
SOLID_ANGLE_UNIT()
);
#11827=SHAPE_DEFINITION_REPRESENTATION(#11868,#11966);
#11868=PRODUCT_DEFINITION_SHAPE('',$,#12006);
#11966=SHAPE_REPRESENTATION('',(#7001),#11783);
#11984=PRODUCT_DEFINITION_CONTEXT('part definition',#12103,'design');
#12006=PRODUCT_DEFINITION('M8x25 Bolt','M8x25 Bolt',#12045,#11984);
#12045=PRODUCT_DEFINITION_FORMATION('',$,#12126);
#12103=APPLICATION_CONTEXT(
'Core Data for Automotive Mechanical Design Process');
#12104=PRODUCT_CONTEXT('part definition',#12103,'mechanical');
#12126=PRODUCT('M8x25 Bolt','M8x25 Bolt','M8x25 Bolt',(#12104));
#12214=COLOUR_RGB('Black',0.12,0.14,0.17);
#12215=FILL_AREA_STYLE_COLOUR('',#12214);
#12216=FILL_AREA_STYLE('',(#12215));
#12217=SURFACE_STYLE_FILL_AREA(#12216);
#12218=SURFACE_SIDE_STYLE('',(#12217));
#12219=SURFACE_STYLE_USAGE(.BOTH.,#12218);
#12220=PRESENTATION_STYLE_ASSIGNMENT((#12219));
ENDSEC;
END-ISO-10303-21;
